ISO-10303-21;
HEADER;
/* Generated by software containing ST-Developer
 * from STEP Tools, Inc. (www.steptools.com) 
 */

FILE_DESCRIPTION(
/* description */ ('Belt tension measurement rig'),
/* implementation_level */ '2;1');

FILE_NAME(
/* name */ 'M4x10 Cap Screw.step',
/* time_stamp */ '2026-10-28T03:24:44-07:00',
/* author */ (''),
/* organization */ (''),
/* preprocessor_version */ 'ST-DEVELOPER v20.2',
/* originating_system */ 'Autodesk Translation Framework v15.17.0.0',
/* authorisation */ '');

FILE_SCHEMA (('AUTOMOTIVE_DESIGN { 1 0 10303 214 3 1 1 }'));
ENDSEC;

DATA;
#10=MECHANICAL_DESIGN_GEOMETRIC_PRESENTATION_REPRESENTATION('',(#743),#23587);
#12=ORIENTED_CLOSED_SHELL('',*,#12249,.F.);
#15=BREP_WITH_VOIDS('Body1',#12250,(#12));
#478=CONICAL_SURFACE('',#13794,0.325,0.785398163397448);
#479=CONICAL_SURFACE('',#13798,0.335,0.785398163397448);
#480=CONICAL_SURFACE('',#13802,0.21,0.463647609000806);
#618=SHAPE_REPRESENTATION_RELATIONSHIP('SRR','None',#23867,#673);
#673=ADVANCED_BREP_SHAPE_REPRESENTATION('',(#15),#23565);
#743=STYLED_ITEM('',(#24218),#15);
#983=FACE_BOUND('',#2655,.T.);
#1266=PLANE('',#13782);
#1267=PLANE('',#13783);
#1268=PLANE('',#13784);
#1269=PLANE('',#13785);
#1270=PLANE('',#13786);
#1271=PLANE('',#13787);
#1272=PLANE('',#13788);
#1273=PLANE('',#13789);
#1274=PLANE('',#13790);
#1275=PLANE('',#13792);
#1276=PLANE('',#13800);
#1783=FACE_OUTER_BOUND('',#2641,.T.);
#1784=FACE_OUTER_BOUND('',#2642,.T.);
#1785=FACE_OUTER_BOUND('',#2643,.T.);
#1786=FACE_OUTER_BOUND('',#2644,.T.);
#1787=FACE_OUTER_BOUND('',#2645,.T.);
#1788=FACE_OUTER_BOUND('',#2646,.T.);
#1789=FACE_OUTER_BOUND('',#2647,.T.);
#1790=FACE_OUTER_BOUND('',#2648,.T.);
#1791=FACE_OUTER_BOUND('',#2649,.T.);
#1792=FACE_OUTER_BOUND('',#2650,.T.);
#1793=FACE_OUTER_BOUND('',#2651,.T.);
#1794=FACE_OUTER_BOUND('',#2652,.T.);
#1795=FACE_OUTER_BOUND('',#2653,.T.);
#1796=FACE_OUTER_BOUND('',#2654,.T.);
#1797=FACE_OUTER_BOUND('',#2656,.T.);
#1798=FACE_OUTER_BOUND('',#2657,.T.);
#2641=EDGE_LOOP('',(#9860,#9861,#9862,#9863));
#2642=EDGE_LOOP('',(#9864,#9865,#9866,#9867));
#2643=EDGE_LOOP('',(#9868,#9869,#9870,#9871));
#2644=EDGE_LOOP('',(#9872,#9873,#9874,#9875));
#2645=EDGE_LOOP('',(#9876,#9877,#9878,#9879));
#2646=EDGE_LOOP('',(#9880,#9881,#9882,#9883));
#2647=EDGE_LOOP('',(#9884,#9885,#9886,#9887,#9888,#9889));
#2648=EDGE_LOOP('',(#9890,#9891,#9892,#9893,#9894,#9895));
#2649=EDGE_LOOP('',(#9896));
#2650=EDGE_LOOP('',(#9897));
#2651=EDGE_LOOP('',(#9898,#9899,#9900,#9901));
#2652=EDGE_LOOP('',(#9902,#9903,#9904,#9905));
#2653=EDGE_LOOP('',(#9906,#9907,#9908,#9909));
#2654=EDGE_LOOP('',(#9910));
#2655=EDGE_LOOP('',(#9911));
#2656=EDGE_LOOP('',(#9912,#9913,#9914,#9915));
#2657=EDGE_LOOP('',(#9916,#9917,#9918,#9919));
#3470=LINE('',#21379,#4221);
#3471=LINE('',#21381,#4222);
#3472=LINE('',#21383,#4223);
#3473=LINE('',#21384,#4224);
#3474=LINE('',#21387,#4225);
#3475=LINE('',#21389,#4226);
#3476=LINE('',#21390,#4227);
#3477=LINE('',#21393,#4228);
#3478=LINE('',#21395,#4229);
#3479=LINE('',#21396,#4230);
#3480=LINE('',#21399,#4231);
#3481=LINE('',#21401,#4232);
#3482=LINE('',#21402,#4233);
#3483=LINE('',#21405,#4234);
#3484=LINE('',#21407,#4235);
#3485=LINE('',#21408,#4236);
#3486=LINE('',#21410,#4237);
#3487=LINE('',#21411,#4238);
#3488=LINE('',#21423,#4239);
#3489=LINE('',#21427,#4240);
#3490=LINE('',#21431,#4241);
#3491=LINE('',#21438,#4242);
#3492=LINE('',#21440,#4243);
#4221=VECTOR('',#16833,1.);
#4222=VECTOR('',#16834,1.);
#4223=VECTOR('',#16835,1.);
#4224=VECTOR('',#16836,1.);
#4225=VECTOR('',#16839,1.);
#4226=VECTOR('',#16840,1.);
#4227=VECTOR('',#16841,1.);
#4228=VECTOR('',#16844,1.);
#4229=VECTOR('',#16845,1.);
#4230=VECTOR('',#16846,1.);
#4231=VECTOR('',#16849,1.);
#4232=VECTOR('',#16850,1.);
#4233=VECTOR('',#16851,1.);
#4234=VECTOR('',#16854,1.);
#4235=VECTOR('',#16855,1.);
#4236=VECTOR('',#16856,1.);
#4237=VECTOR('',#16859,1.);
#4238=VECTOR('',#16860,1.);
#4239=VECTOR('',#16877,0.325);
#4240=VECTOR('',#16882,0.35);
#4241=VECTOR('',#16887,0.335);
#4242=VECTOR('',#16896,0.21);
#4243=VECTOR('',#16899,0.2);
#4889=CIRCLE('',#13791,0.1954);
#4890=CIRCLE('',#13793,0.3);
#4891=CIRCLE('',#13795,0.35);
#4892=CIRCLE('',#13797,0.35);
#4893=CIRCLE('',#13799,0.32);
#4894=CIRCLE('',#13801,0.22);
#4895=CIRCLE('',#13803,0.1954);
#5892=VERTEX_POINT('',#21377);
#5893=VERTEX_POINT('',#21378);
#5894=VERTEX_POINT('',#21380);
#5895=VERTEX_POINT('',#21382);
#5896=VERTEX_POINT('',#21386);
#5897=VERTEX_POINT('',#21388);
#5898=VERTEX_POINT('',#21392);
#5899=VERTEX_POINT('',#21394);
#5900=VERTEX_POINT('',#21398);
#5901=VERTEX_POINT('',#21400);
#5902=VERTEX_POINT('',#21404);
#5903=VERTEX_POINT('',#21406);
#5904=VERTEX_POINT('',#21415);
#5905=VERTEX_POINT('',#21418);
#5906=VERTEX_POINT('',#21421);
#5907=VERTEX_POINT('',#21425);
#5908=VERTEX_POINT('',#21429);
#5909=VERTEX_POINT('',#21433);
#5910=VERTEX_POINT('',#21436);
#7289=EDGE_CURVE('',#5892,#5893,#3470,.T.);
#7290=EDGE_CURVE('',#5893,#5894,#3471,.T.);
#7291=EDGE_CURVE('',#5894,#5895,#3472,.T.);
#7292=EDGE_CURVE('',#5892,#5895,#3473,.T.);
#7293=EDGE_CURVE('',#5893,#5896,#3474,.T.);
#7294=EDGE_CURVE('',#5896,#5897,#3475,.T.);
#7295=EDGE_CURVE('',#5897,#5894,#3476,.T.);
#7296=EDGE_CURVE('',#5896,#5898,#3477,.T.);
#7297=EDGE_CURVE('',#5898,#5899,#3478,.T.);
#7298=EDGE_CURVE('',#5899,#5897,#3479,.T.);
#7299=EDGE_CURVE('',#5898,#5900,#3480,.T.);
#7300=EDGE_CURVE('',#5900,#5901,#3481,.T.);
#7301=EDGE_CURVE('',#5901,#5899,#3482,.T.);
#7302=EDGE_CURVE('',#5900,#5902,#3483,.T.);
#7303=EDGE_CURVE('',#5902,#5903,#3484,.T.);
#7304=EDGE_CURVE('',#5903,#5901,#3485,.T.);
#7305=EDGE_CURVE('',#5902,#5892,#3486,.T.);
#7306=EDGE_CURVE('',#5895,#5903,#3487,.T.);
#7307=EDGE_CURVE('',#5904,#5904,#4889,.T.);
#7308=EDGE_CURVE('',#5905,#5905,#4890,.T.);
#7309=EDGE_CURVE('',#5906,#5906,#4891,.T.);
#7310=EDGE_CURVE('',#5906,#5905,#3488,.T.);
#7311=EDGE_CURVE('',#5907,#5907,#4892,.T.);
#7312=EDGE_CURVE('',#5907,#5906,#3489,.T.);
#7313=EDGE_CURVE('',#5908,#5908,#4893,.T.);
#7314=EDGE_CURVE('',#5908,#5907,#3490,.T.);
#7315=EDGE_CURVE('',#5909,#5909,#4894,.T.);
#7316=EDGE_CURVE('',#5910,#5910,#4895,.F.);
#7317=EDGE_CURVE('',#5910,#5909,#3491,.T.);
#7318=EDGE_CURVE('',#5904,#5910,#3492,.T.);
#9860=ORIENTED_EDGE('',*,*,#7289,.T.);
#9861=ORIENTED_EDGE('',*,*,#7290,.T.);
#9862=ORIENTED_EDGE('',*,*,#7291,.T.);
#9863=ORIENTED_EDGE('',*,*,#7292,.F.);
#9864=ORIENTED_EDGE('',*,*,#7293,.T.);
#9865=ORIENTED_EDGE('',*,*,#7294,.T.);
#9866=ORIENTED_EDGE('',*,*,#7295,.T.);
#9867=ORIENTED_EDGE('',*,*,#7290,.F.);
#9868=ORIENTED_EDGE('',*,*,#7296,.T.);
#9869=ORIENTED_EDGE('',*,*,#7297,.T.);
#9870=ORIENTED_EDGE('',*,*,#7298,.T.);
#9871=ORIENTED_EDGE('',*,*,#7294,.F.);
#9872=ORIENTED_EDGE('',*,*,#7299,.T.);
#9873=ORIENTED_EDGE('',*,*,#7300,.T.);
#9874=ORIENTED_EDGE('',*,*,#7301,.T.);
#9875=ORIENTED_EDGE('',*,*,#7297,.F.);
#9876=ORIENTED_EDGE('',*,*,#7302,.T.);
#9877=ORIENTED_EDGE('',*,*,#7303,.T.);
#9878=ORIENTED_EDGE('',*,*,#7304,.T.);
#9879=ORIENTED_EDGE('',*,*,#7300,.F.);
#9880=ORIENTED_EDGE('',*,*,#7305,.T.);
#9881=ORIENTED_EDGE('',*,*,#7292,.T.);
#9882=ORIENTED_EDGE('',*,*,#7306,.T.);
#9883=ORIENTED_EDGE('',*,*,#7303,.F.);
#9884=ORIENTED_EDGE('',*,*,#7305,.F.);
#9885=ORIENTED_EDGE('',*,*,#7302,.F.);
#9886=ORIENTED_EDGE('',*,*,#7299,.F.);
#9887=ORIENTED_EDGE('',*,*,#7296,.F.);
#9888=ORIENTED_EDGE('',*,*,#7293,.F.);
#9889=ORIENTED_EDGE('',*,*,#7289,.F.);
#9890=ORIENTED_EDGE('',*,*,#7306,.F.);
#9891=ORIENTED_EDGE('',*,*,#7291,.F.);
#9892=ORIENTED_EDGE('',*,*,#7295,.F.);
#9893=ORIENTED_EDGE('',*,*,#7298,.F.);
#9894=ORIENTED_EDGE('',*,*,#7301,.F.);
#9895=ORIENTED_EDGE('',*,*,#7304,.F.);
#9896=ORIENTED_EDGE('',*,*,#7307,.F.);
#9897=ORIENTED_EDGE('',*,*,#7308,.F.);
#9898=ORIENTED_EDGE('',*,*,#7309,.F.);
#9899=ORIENTED_EDGE('',*,*,#7310,.T.);
#9900=ORIENTED_EDGE('',*,*,#7308,.T.);
#9901=ORIENTED_EDGE('',*,*,#7310,.F.);
#9902=ORIENTED_EDGE('',*,*,#7311,.F.);
#9903=ORIENTED_EDGE('',*,*,#7312,.T.);
#9904=ORIENTED_EDGE('',*,*,#7309,.T.);
#9905=ORIENTED_EDGE('',*,*,#7312,.F.);
#9906=ORIENTED_EDGE('',*,*,#7313,.F.);
#9907=ORIENTED_EDGE('',*,*,#7314,.T.);
#9908=ORIENTED_EDGE('',*,*,#7311,.T.);
#9909=ORIENTED_EDGE('',*,*,#7314,.F.);
#9910=ORIENTED_EDGE('',*,*,#7313,.T.);
#9911=ORIENTED_EDGE('',*,*,#7315,.F.);
#9912=ORIENTED_EDGE('',*,*,#7316,.F.);
#9913=ORIENTED_EDGE('',*,*,#7317,.T.);
#9914=ORIENTED_EDGE('',*,*,#7315,.T.);
#9915=ORIENTED_EDGE('',*,*,#7317,.F.);
#9916=ORIENTED_EDGE('',*,*,#7307,.T.);
#9917=ORIENTED_EDGE('',*,*,#7318,.T.);
#9918=ORIENTED_EDGE('',*,*,#7316,.T.);
#9919=ORIENTED_EDGE('',*,*,#7318,.F.);
#11315=CYLINDRICAL_SURFACE('',#13796,0.35);
#11316=CYLINDRICAL_SURFACE('',#13804,0.1954);
#11924=ADVANCED_FACE('',(#1783),#1266,.F.);
#11925=ADVANCED_FACE('',(#1784),#1267,.F.);
#11926=ADVANCED_FACE('',(#1785),#1268,.F.);
#11927=ADVANCED_FACE('',(#1786),#1269,.F.);
#11928=ADVANCED_FACE('',(#1787),#1270,.F.);
#11929=ADVANCED_FACE('',(#1788),#1271,.F.);
#11930=ADVANCED_FACE('',(#1789),#1272,.F.);
#11931=ADVANCED_FACE('',(#1790),#1273,.F.);
#11932=ADVANCED_FACE('',(#1791),#1274,.F.);
#11933=ADVANCED_FACE('',(#1792),#1275,.T.);
#11934=ADVANCED_FACE('',(#1793),#478,.T.);
#11935=ADVANCED_FACE('',(#1794),#11315,.T.);
#11936=ADVANCED_FACE('',(#1795),#479,.T.);
#11937=ADVANCED_FACE('',(#1796,#983),#1276,.T.);
#11938=ADVANCED_FACE('',(#1797),#480,.T.);
#11939=ADVANCED_FACE('',(#1798),#11316,.T.);
#12249=CLOSED_SHELL('',(#11924,#11925,#11926,#11927,#11928,#11929,#11930,
#11931));
#12250=CLOSED_SHELL('',(#11932,#11933,#11934,#11935,#11936,#11937,#11938,
#11939));
#13781=AXIS2_PLACEMENT_3D('',#21375,#16829,#16830);
#13782=AXIS2_PLACEMENT_3D('',#21376,#16831,#16832);
#13783=AXIS2_PLACEMENT_3D('',#21385,#16837,#16838);
#13784=AXIS2_PLACEMENT_3D('',#21391,#16842,#16843);
#13785=AXIS2_PLACEMENT_3D('',#21397,#16847,#16848);
#13786=AXIS2_PLACEMENT_3D('',#21403,#16852,#16853);
#13787=AXIS2_PLACEMENT_3D('',#21409,#16857,#16858);
#13788=AXIS2_PLACEMENT_3D('',#21412,#16861,#16862);
#13789=AXIS2_PLACEMENT_3D('',#21413,#16863,#16864);
#13790=AXIS2_PLACEMENT_3D('',#21414,#16865,#16866);
#13791=AXIS2_PLACEMENT_3D('',#21416,#16867,#16868);
#13792=AXIS2_PLACEMENT_3D('',#21417,#16869,#16870);
#13793=AXIS2_PLACEMENT_3D('',#21419,#16871,#16872);
#13794=AXIS2_PLACEMENT_3D('',#21420,#16873,#16874);
#13795=AXIS2_PLACEMENT_3D('',#21422,#16875,#16876);
#13796=AXIS2_PLACEMENT_3D('',#21424,#16878,#16879);
#13797=AXIS2_PLACEMENT_3D('',#21426,#16880,#16881);
#13798=AXIS2_PLACEMENT_3D('',#21428,#16883,#16884);
#13799=AXIS2_PLACEMENT_3D('',#21430,#16885,#16886);
#13800=AXIS2_PLACEMENT_3D('',#21432,#16888,#16889);
#13801=AXIS2_PLACEMENT_3D('',#21434,#16890,#16891);
#13802=AXIS2_PLACEMENT_3D('',#21435,#16892,#16893);
#13803=AXIS2_PLACEMENT_3D('',#21437,#16894,#16895);
#13804=AXIS2_PLACEMENT_3D('',#21439,#16897,#16898);
#16829=DIRECTION('axis',(0.,0.,1.));
#16830=DIRECTION('refdir',(1.,0.,0.));
#16831=DIRECTION('center_axis',(0.866025403784439,0.,-0.5));
#16832=DIRECTION('ref_axis',(0.5,0.,0.866025403784439));
#16833=DIRECTION('',(-0.5,0.,-0.866025403784439));
#16834=DIRECTION('',(0.,-1.,0.));
#16835=DIRECTION('',(0.5,0.,0.866025403784439));
#16836=DIRECTION('',(0.,-1.,0.));
#16837=DIRECTION('center_axis',(1.60246890531964E-16,0.,-1.));
#16838=DIRECTION('ref_axis',(1.,0.,1.60246890531964E-16));
#16839=DIRECTION('',(-1.,0.,-1.60246890531964E-16));
#16840=DIRECTION('',(0.,-1.,0.));
#16841=DIRECTION('',(1.,0.,1.60246890531964E-16));
#16842=DIRECTION('center_axis',(-0.866025403784439,0.,-0.5));
#16843=DIRECTION('ref_axis',(0.5,0.,-0.866025403784439));
#16844=DIRECTION('',(-0.5,0.,0.866025403784439));
#16845=DIRECTION('',(0.,-1.,0.));
#16846=DIRECTION('',(0.5,0.,-0.866025403784439));
#16847=DIRECTION('center_axis',(-0.866025403784439,0.,0.5));
#16848=DIRECTION('ref_axis',(-0.5,0.,-0.866025403784439));
#16849=DIRECTION('',(0.5,0.,0.866025403784439));
#16850=DIRECTION('',(0.,-1.,0.));
#16851=DIRECTION('',(-0.5,0.,-0.866025403784439));
#16852=DIRECTION('center_axis',(-1.60246890531964E-16,0.,1.));
#16853=DIRECTION('ref_axis',(-1.,0.,-1.60246890531964E-16));
#16854=DIRECTION('',(1.,0.,1.60246890531964E-16));
#16855=DIRECTION('',(0.,-1.,0.));
#16856=DIRECTION('',(-1.,0.,-1.60246890531964E-16));
#16857=DIRECTION('center_axis',(0.866025403784439,0.,0.5));
#16858=DIRECTION('ref_axis',(-0.5,0.,0.866025403784439));
#16859=DIRECTION('',(0.5,0.,-0.866025403784439));
#16860=DIRECTION('',(-0.5,0.,0.866025403784439));
#16861=DIRECTION('center_axis',(0.,1.,0.));
#16862=DIRECTION('ref_axis',(1.,0.,0.));
#16863=DIRECTION('center_axis',(0.,-1.,0.));
#16864=DIRECTION('ref_axis',(0.,0.,-1.));
#16865=DIRECTION('center_axis',(0.,1.,0.));
#16866=DIRECTION('ref_axis',(1.,0.,0.));
#16867=DIRECTION('center_axis',(0.,1.,0.));
#16868=DIRECTION('ref_axis',(1.,0.,0.));
#16869=DIRECTION('center_axis',(0.,1.,0.));
#16870=DIRECTION('ref_axis',(0.,0.,1.));
#16871=DIRECTION('center_axis',(0.,-1.,0.));
#16872=DIRECTION('ref_axis',(1.,0.,0.));
#16873=DIRECTION('center_axis',(0.,-1.,0.));
#16874=DIRECTION('ref_axis',(1.,0.,0.));
#16875=DIRECTION('center_axis',(0.,-1.,0.));
#16876=DIRECTION('ref_axis',(1.,0.,0.));
#16877=DIRECTION('',(0.707106781186547,0.707106781186548,8.65956056235493E-17));
#16878=DIRECTION('center_axis',(0.,-1.,0.));
#16879=DIRECTION('ref_axis',(1.,0.,0.));
#16880=DIRECTION('center_axis',(0.,-1.,0.));
#16881=DIRECTION('ref_axis',(1.,0.,0.));
#16882=DIRECTION('',(0.,1.,0.));
#16883=DIRECTION('center_axis',(0.,1.,0.));
#16884=DIRECTION('ref_axis',(1.,0.,0.));
#16885=DIRECTION('center_axis',(0.,-1.,0.));
#16886=DIRECTION('ref_axis',(1.,0.,0.));
#16887=DIRECTION('',(-0.707106781186547,0.707106781186548,-8.65956056235493E-17));
#16888=DIRECTION('center_axis',(0.,-1.,0.));
#16889=DIRECTION('ref_axis',(0.,0.,-1.));
#16890=DIRECTION('center_axis',(0.,-1.,0.));
#16891=DIRECTION('ref_axis',(1.,0.,0.));
#16892=DIRECTION('center_axis',(0.,1.,0.));
#16893=DIRECTION('ref_axis',(1.,0.,0.));
#16894=DIRECTION('center_axis',(0.,1.,0.));
#16895=DIRECTION('ref_axis',(1.,0.,0.));
#16896=DIRECTION('',(-0.447213595499958,0.894427190999916,-5.47678698264203E-17));
#16897=DIRECTION('center_axis',(0.,-1.,0.));
#16898=DIRECTION('ref_axis',(1.,0.,0.));
#16899=DIRECTION('',(0.,1.,0.));
#21375=CARTESIAN_POINT('',(0.,0.,0.));
#21376=CARTESIAN_POINT('Origin',(0.0866025403784439,-0.4,-0.15));
#21377=CARTESIAN_POINT('',(0.173205080756888,-0.4,0.));
#21378=CARTESIAN_POINT('',(0.0866025403784439,-0.4,-0.15));
#21379=CARTESIAN_POINT('',(0.173205080756888,-0.4,0.));
#21380=CARTESIAN_POINT('',(0.0866025403784439,-0.64,-0.15));
#21381=CARTESIAN_POINT('',(0.0866025403784439,-0.4,-0.15));
#21382=CARTESIAN_POINT('',(0.173205080756888,-0.64,0.));
#21383=CARTESIAN_POINT('',(0.173205080756888,-0.64,0.));
#21384=CARTESIAN_POINT('',(0.173205080756888,-0.4,0.));
#21385=CARTESIAN_POINT('Origin',(-0.0866025403784438,-0.4,-0.15));
#21386=CARTESIAN_POINT('',(-0.0866025403784438,-0.4,-0.15));
#21387=CARTESIAN_POINT('',(0.0866025403784439,-0.4,-0.15));
#21388=CARTESIAN_POINT('',(-0.0866025403784438,-0.64,-0.15));
#21389=CARTESIAN_POINT('',(-0.0866025403784438,-0.4,-0.15));
#21390=CARTESIAN_POINT('',(0.0866025403784439,-0.64,-0.15));
#21391=CARTESIAN_POINT('Origin',(-0.173205080756888,-0.4,-2.77555756156289E-17));
#21392=CARTESIAN_POINT('',(-0.173205080756888,-0.4,-2.12115047744981E-17));
#21393=CARTESIAN_POINT('',(-0.0866025403784438,-0.4,-0.15));
#21394=CARTESIAN_POINT('',(-0.173205080756888,-0.64,-2.77555756156289E-17));
#21395=CARTESIAN_POINT('',(-0.173205080756888,-0.4,-2.12115047744981E-17));
#21396=CARTESIAN_POINT('',(-0.0866025403784438,-0.64,-0.15));
#21397=CARTESIAN_POINT('Origin',(-0.0866025403784439,-0.4,0.15));
#21398=CARTESIAN_POINT('',(-0.0866025403784439,-0.4,0.15));
#21399=CARTESIAN_POINT('',(-0.173205080756888,-0.4,-2.12115047744981E-17));
#21400=CARTESIAN_POINT('',(-0.0866025403784439,-0.64,0.15));
#21401=CARTESIAN_POINT('',(-0.0866025403784439,-0.4,0.15));
#21402=CARTESIAN_POINT('',(-0.173205080756888,-0.64,-2.12115047744981E-17));
#21403=CARTESIAN_POINT('Origin',(0.0866025403784439,-0.4,0.15));
#21404=CARTESIAN_POINT('',(0.0866025403784439,-0.4,0.15));
#21405=CARTESIAN_POINT('',(-0.0866025403784439,-0.4,0.15));
#21406=CARTESIAN_POINT('',(0.0866025403784439,-0.64,0.15));
#21407=CARTESIAN_POINT('',(0.0866025403784439,-0.4,0.15));
#21408=CARTESIAN_POINT('',(-0.0866025403784439,-0.64,0.15));
#21409=CARTESIAN_POINT('Origin',(0.173205080756888,-0.4,0.));
#21410=CARTESIAN_POINT('',(0.0866025403784439,-0.4,0.15));
#21411=CARTESIAN_POINT('',(0.0866025403784439,-0.64,0.15));
#21412=CARTESIAN_POINT('Origin',(0.,-0.4,-2.77555756156289E-17));
#21413=CARTESIAN_POINT('Origin',(0.,-0.64,-2.77555756156289E-17));
#21414=CARTESIAN_POINT('Origin',(0.,-1.,0.));
#21415=CARTESIAN_POINT('',(-0.1954,-1.,2.39295984553393E-17));
#21416=CARTESIAN_POINT('Origin',(0.,-1.,0.));
#21417=CARTESIAN_POINT('Origin',(0.3,0.4,0.));
#21418=CARTESIAN_POINT('',(-0.3,0.4,-3.67394039744206E-17));
#21419=CARTESIAN_POINT('Origin',(0.,0.4,0.));
#21420=CARTESIAN_POINT('Origin',(0.,0.375,0.));
#21421=CARTESIAN_POINT('',(-0.35,0.35,-4.28626379701573E-17));
#21422=CARTESIAN_POINT('Origin',(0.,0.35,0.));
#21423=CARTESIAN_POINT('',(-0.325,0.375,-3.9801020972289E-17));
#21424=CARTESIAN_POINT('Origin',(0.,0.19,0.));
#21425=CARTESIAN_POINT('',(-0.35,0.03,-4.28626379701574E-17));
#21426=CARTESIAN_POINT('Origin',(0.,0.03,0.));
#21427=CARTESIAN_POINT('',(-0.35,0.19,-4.28626379701574E-17));
#21428=CARTESIAN_POINT('Origin',(0.,0.0149999999999999,0.));
#21429=CARTESIAN_POINT('',(-0.32,-3.29597460435593E-17,-3.91886975727153E-17));
#21430=CARTESIAN_POINT('Origin',(0.,0.,0.));
#21431=CARTESIAN_POINT('',(-0.335,0.0149999999999999,-4.10256677714363E-17));
#21432=CARTESIAN_POINT('Origin',(0.22,0.,0.));
#21433=CARTESIAN_POINT('',(-0.22,-6.93889390390723E-18,-2.69422295812418E-17));
#21434=CARTESIAN_POINT('Origin',(0.,0.,0.));
#21435=CARTESIAN_POINT('Origin',(0.,-0.02,0.));
#21436=CARTESIAN_POINT('',(-0.1954,-0.0492,2.39295984553393E-17));
#21437=CARTESIAN_POINT('Origin',(0.,-0.0492,0.));
#21438=CARTESIAN_POINT('',(-0.21,-0.02,-2.57175827820944E-17));
#21439=CARTESIAN_POINT('Origin',(0.,-0.8,0.));
#21440=CARTESIAN_POINT('',(-0.1954,-0.8,-2.39295984553393E-17));
#23500=UNCERTAINTY_MEASURE_WITH_UNIT(LENGTH_MEASURE(0.001),#23588,
'DISTANCE_ACCURACY_VALUE',
'Maximum model space distance between geometric entities at asserted c
onnectivities');
#23522=UNCERTAINTY_MEASURE_WITH_UNIT(LENGTH_MEASURE(0.001),#23588,
'DISTANCE_ACCURACY_VALUE',
'Maximum model space distance between geometric entities at asserted c
onnectivities');
#23565=(
GEOMETRIC_REPRESENTATION_CONTEXT(3)
GLOBAL_UNCERTAINTY_ASSIGNED_CONTEXT((#23500))
GLOBAL_UNIT_ASSIGNED_CONTEXT((#23588,#23590,#23591))
REPRESENTATION_CONTEXT('','3D')
);
#23587=(
GEOMETRIC_REPRESENTATION_CONTEXT(3)
GLOBAL_UNCERTAINTY_ASSIGNED_CONTEXT((#23522))
GLOBAL_UNIT_ASSIGNED_CONTEXT((#23588,#23590,#23591))
REPRESENTATION_CONTEXT('','3D')
);
#23588=(
LENGTH_UNIT()
NAMED_UNIT(*)
SI_UNIT(.CENTI.,.METRE.)
);
#23590=(
NAMED_UNIT(*)
PLANE_ANGLE_UNIT()
SI_UNIT($,.RADIAN.)
);
#23591=(
NAMED_UNIT(*)
SI_UNIT($,.STERADIAN.)
SOLID_ANGLE_UNIT()
);
#23634=SHAPE_DEFINITION_REPRESENTATION(#23711,#23867);
#23711=PRODUCT_DEFINITION_SHAPE('',$,#23932);
#23867=SHAPE_REPRESENTATION('',(#13781),#23565);
#23889=PRODUCT_DEFINITION_CONTEXT('part definition',#24083,'design');
#23932=PRODUCT_DEFINITION('M4x10 Cap Screw','M4x10 Cap Screw',#23996,#23889);
#23996=PRODUCT_DEFINITION_FORMATION('',$,#24127);
#24083=APPLICATION_CONTEXT(
'Core Data for Automotive Mechanical Design Process');
#24084=PRODUCT_CONTEXT('part definition',#24083,'mechanical');
#24127=PRODUCT('M4x10 Cap Screw','M4x10 Cap Screw','M4x10 Cap Screw',(#24084));
#24212=COLOUR_RGB('Black',0.12,0.14,0.17);
#24213=FILL_AREA_STYLE_COLOUR('',#24212);
#24214=FILL_AREA_STYLE('',(#24213));
#24215=SURFACE_STYLE_FILL_AREA(#24214);
#24216=SURFACE_SIDE_STYLE('',(#24215));
#24217=SURFACE_STYLE_USAGE(.BOTH.,#24216);
#24218=PRESENTATION_STYLE_ASSIGNMENT((#24217));
ENDSEC;
END-ISO-10303-21;
